ISO-10303-21;
HEADER;
/* Generated by software containing ST-Developer
 * from STEP Tools, Inc. (www.steptools.com) 
 */

FILE_DESCRIPTION(
/* description */ ('Bearing friction torque test rig'),
/* implementation_level */ '2;1');

FILE_NAME(
/* name */ 'M6x18 mounting screw.step',
/* time_stamp */ '2026-10-28T03:24:04-07:00',
/* author */ (''),
/* organization */ (''),
/* preprocessor_version */ 'ST-DEVELOPER v20.2',
/* originating_system */ 'Autodesk Translation Framework v15.17.0.0',
/* authorisation */ '');

FILE_SCHEMA (('AUTOMOTIVE_DESIGN { 1 0 10303 214 3 1 1 }'));
ENDSEC;

DATA;
#10=MECHANICAL_DESIGN_GEOMETRIC_PRESENTATION_REPRESENTATION('',(#554),#14822);
#429=CONICAL_SURFACE('',#8611,0.475,0.785398163397449);
#430=CONICAL_SURFACE('',#8615,0.485,0.785398163397448);
#431=CONICAL_SURFACE('',#8619,0.31,0.463647609000806);
#449=ORIENTED_CLOSED_SHELL('',*,#7670,.F.);
#452=BREP_WITH_VOIDS('Body1',#7671,(#449));
#476=SHAPE_REPRESENTATION_RELATIONSHIP('SRR','None',#15015,#515);
#515=ADVANCED_BREP_SHAPE_REPRESENTATION('',(#452),#14795);
#554=STYLED_ITEM('',(#15291),#452);
#813=FACE_BOUND('',#1948,.T.);
#991=PLANE('',#8599);
#992=PLANE('',#8600);
#993=PLANE('',#8601);
#994=PLANE('',#8602);
#995=PLANE('',#8603);
#996=PLANE('',#8604);
#997=PLANE('',#8605);
#998=PLANE('',#8606);
#999=PLANE('',#8607);
#1000=PLANE('',#8609);
#1001=PLANE('',#8617);
#1320=FACE_OUTER_BOUND('',#1934,.T.);
#1321=FACE_OUTER_BOUND('',#1935,.T.);
#1322=FACE_OUTER_BOUND('',#1936,.T.);
#1323=FACE_OUTER_BOUND('',#1937,.T.);
#1324=FACE_OUTER_BOUND('',#1938,.T.);
#1325=FACE_OUTER_BOUND('',#1939,.T.);
#1326=FACE_OUTER_BOUND('',#1940,.T.);
#1327=FACE_OUTER_BOUND('',#1941,.T.);
#1328=FACE_OUTER_BOUND('',#1942,.T.);
#1329=FACE_OUTER_BOUND('',#1943,.T.);
#1330=FACE_OUTER_BOUND('',#1944,.T.);
#1331=FACE_OUTER_BOUND('',#1945,.T.);
#1332=FACE_OUTER_BOUND('',#1946,.T.);
#1333=FACE_OUTER_BOUND('',#1947,.T.);
#1334=FACE_OUTER_BOUND('',#1949,.T.);
#1335=FACE_OUTER_BOUND('',#1950,.T.);
#1934=EDGE_LOOP('',(#6144,#6145,#6146,#6147));
#1935=EDGE_LOOP('',(#6148,#6149,#6150,#6151));
#1936=EDGE_LOOP('',(#6152,#6153,#6154,#6155));
#1937=EDGE_LOOP('',(#6156,#6157,#6158,#6159));
#1938=EDGE_LOOP('',(#6160,#6161,#6162,#6163));
#1939=EDGE_LOOP('',(#6164,#6165,#6166,#6167));
#1940=EDGE_LOOP('',(#6168,#6169,#6170,#6171,#6172,#6173));
#1941=EDGE_LOOP('',(#6174,#6175,#6176,#6177,#6178,#6179));
#1942=EDGE_LOOP('',(#6180));
#1943=EDGE_LOOP('',(#6181));
#1944=EDGE_LOOP('',(#6182,#6183,#6184,#6185));
#1945=EDGE_LOOP('',(#6186,#6187,#6188,#6189));
#1946=EDGE_LOOP('',(#6190,#6191,#6192,#6193));
#1947=EDGE_LOOP('',(#6194));
#1948=EDGE_LOOP('',(#6195));
#1949=EDGE_LOOP('',(#6196,#6197,#6198,#6199));
#1950=EDGE_LOOP('',(#6200,#6201,#6202,#6203));
#2499=LINE('',#12730,#2943);
#2500=LINE('',#12732,#2944);
#2501=LINE('',#12734,#2945);
#2502=LINE('',#12735,#2946);
#2503=LINE('',#12738,#2947);
#2504=LINE('',#12740,#2948);
#2505=LINE('',#12741,#2949);
#2506=LINE('',#12744,#2950);
#2507=LINE('',#12746,#2951);
#2508=LINE('',#12747,#2952);
#2509=LINE('',#12750,#2953);
#2510=LINE('',#12752,#2954);
#2511=LINE('',#12753,#2955);
#2512=LINE('',#12756,#2956);
#2513=LINE('',#12758,#2957);
#2514=LINE('',#12759,#2958);
#2515=LINE('',#12761,#2959);
#2516=LINE('',#12762,#2960);
#2517=LINE('',#12774,#2961);
#2518=LINE('',#12778,#2962);
#2519=LINE('',#12782,#2963);
#2520=LINE('',#12789,#2964);
#2521=LINE('',#12791,#2965);
#2943=VECTOR('',#10362,1.);
#2944=VECTOR('',#10363,1.);
#2945=VECTOR('',#10364,1.);
#2946=VECTOR('',#10365,1.);
#2947=VECTOR('',#10368,1.);
#2948=VECTOR('',#10369,1.);
#2949=VECTOR('',#10370,1.);
#2950=VECTOR('',#10373,1.);
#2951=VECTOR('',#10374,1.);
#2952=VECTOR('',#10375,1.);
#2953=VECTOR('',#10378,1.);
#2954=VECTOR('',#10379,1.);
#2955=VECTOR('',#10380,1.);
#2956=VECTOR('',#10383,1.);
#2957=VECTOR('',#10384,1.);
#2958=VECTOR('',#10385,1.);
#2959=VECTOR('',#10388,1.);
#2960=VECTOR('',#10389,1.);
#2961=VECTOR('',#10406,0.475);
#2962=VECTOR('',#10411,0.5);
#2963=VECTOR('',#10416,0.485);
#2964=VECTOR('',#10425,0.31);
#2965=VECTOR('',#10428,0.3);
#3319=CIRCLE('',#8608,0.2942);
#3320=CIRCLE('',#8610,0.45);
#3321=CIRCLE('',#8612,0.5);
#3322=CIRCLE('',#8614,0.5);
#3323=CIRCLE('',#8616,0.47);
#3324=CIRCLE('',#8618,0.32);
#3325=CIRCLE('',#8620,0.2942);
#3885=VERTEX_POINT('',#12728);
#3886=VERTEX_POINT('',#12729);
#3887=VERTEX_POINT('',#12731);
#3888=VERTEX_POINT('',#12733);
#3889=VERTEX_POINT('',#12737);
#3890=VERTEX_POINT('',#12739);
#3891=VERTEX_POINT('',#12743);
#3892=VERTEX_POINT('',#12745);
#3893=VERTEX_POINT('',#12749);
#3894=VERTEX_POINT('',#12751);
#3895=VERTEX_POINT('',#12755);
#3896=VERTEX_POINT('',#12757);
#3897=VERTEX_POINT('',#12766);
#3898=VERTEX_POINT('',#12769);
#3899=VERTEX_POINT('',#12772);
#3900=VERTEX_POINT('',#12776);
#3901=VERTEX_POINT('',#12780);
#3902=VERTEX_POINT('',#12784);
#3903=VERTEX_POINT('',#12787);
#4698=EDGE_CURVE('',#3885,#3886,#2499,.T.);
#4699=EDGE_CURVE('',#3886,#3887,#2500,.T.);
#4700=EDGE_CURVE('',#3887,#3888,#2501,.T.);
#4701=EDGE_CURVE('',#3885,#3888,#2502,.T.);
#4702=EDGE_CURVE('',#3886,#3889,#2503,.T.);
#4703=EDGE_CURVE('',#3889,#3890,#2504,.T.);
#4704=EDGE_CURVE('',#3890,#3887,#2505,.T.);
#4705=EDGE_CURVE('',#3889,#3891,#2506,.T.);
#4706=EDGE_CURVE('',#3891,#3892,#2507,.T.);
#4707=EDGE_CURVE('',#3892,#3890,#2508,.T.);
#4708=EDGE_CURVE('',#3891,#3893,#2509,.T.);
#4709=EDGE_CURVE('',#3893,#3894,#2510,.T.);
#4710=EDGE_CURVE('',#3894,#3892,#2511,.T.);
#4711=EDGE_CURVE('',#3893,#3895,#2512,.T.);
#4712=EDGE_CURVE('',#3895,#3896,#2513,.T.);
#4713=EDGE_CURVE('',#3896,#3894,#2514,.T.);
#4714=EDGE_CURVE('',#3895,#3885,#2515,.T.);
#4715=EDGE_CURVE('',#3888,#3896,#2516,.T.);
#4716=EDGE_CURVE('',#3897,#3897,#3319,.T.);
#4717=EDGE_CURVE('',#3898,#3898,#3320,.T.);
#4718=EDGE_CURVE('',#3899,#3899,#3321,.T.);
#4719=EDGE_CURVE('',#3899,#3898,#2517,.T.);
#4720=EDGE_CURVE('',#3900,#3900,#3322,.T.);
#4721=EDGE_CURVE('',#3900,#3899,#2518,.T.);
#4722=EDGE_CURVE('',#3901,#3901,#3323,.T.);
#4723=EDGE_CURVE('',#3901,#3900,#2519,.T.);
#4724=EDGE_CURVE('',#3902,#3902,#3324,.T.);
#4725=EDGE_CURVE('',#3903,#3903,#3325,.F.);
#4726=EDGE_CURVE('',#3903,#3902,#2520,.T.);
#4727=EDGE_CURVE('',#3897,#3903,#2521,.T.);
#6144=ORIENTED_EDGE('',*,*,#4698,.T.);
#6145=ORIENTED_EDGE('',*,*,#4699,.T.);
#6146=ORIENTED_EDGE('',*,*,#4700,.T.);
#6147=ORIENTED_EDGE('',*,*,#4701,.F.);
#6148=ORIENTED_EDGE('',*,*,#4702,.T.);
#6149=ORIENTED_EDGE('',*,*,#4703,.T.);
#6150=ORIENTED_EDGE('',*,*,#4704,.T.);
#6151=ORIENTED_EDGE('',*,*,#4699,.F.);
#6152=ORIENTED_EDGE('',*,*,#4705,.T.);
#6153=ORIENTED_EDGE('',*,*,#4706,.T.);
#6154=ORIENTED_EDGE('',*,*,#4707,.T.);
#6155=ORIENTED_EDGE('',*,*,#4703,.F.);
#6156=ORIENTED_EDGE('',*,*,#4708,.T.);
#6157=ORIENTED_EDGE('',*,*,#4709,.T.);
#6158=ORIENTED_EDGE('',*,*,#4710,.T.);
#6159=ORIENTED_EDGE('',*,*,#4706,.F.);
#6160=ORIENTED_EDGE('',*,*,#4711,.T.);
#6161=ORIENTED_EDGE('',*,*,#4712,.T.);
#6162=ORIENTED_EDGE('',*,*,#4713,.T.);
#6163=ORIENTED_EDGE('',*,*,#4709,.F.);
#6164=ORIENTED_EDGE('',*,*,#4714,.T.);
#6165=ORIENTED_EDGE('',*,*,#4701,.T.);
#6166=ORIENTED_EDGE('',*,*,#4715,.T.);
#6167=ORIENTED_EDGE('',*,*,#4712,.F.);
#6168=ORIENTED_EDGE('',*,*,#4714,.F.);
#6169=ORIENTED_EDGE('',*,*,#4711,.F.);
#6170=ORIENTED_EDGE('',*,*,#4708,.F.);
#6171=ORIENTED_EDGE('',*,*,#4705,.F.);
#6172=ORIENTED_EDGE('',*,*,#4702,.F.);
#6173=ORIENTED_EDGE('',*,*,#4698,.F.);
#6174=ORIENTED_EDGE('',*,*,#4715,.F.);
#6175=ORIENTED_EDGE('',*,*,#4700,.F.);
#6176=ORIENTED_EDGE('',*,*,#4704,.F.);
#6177=ORIENTED_EDGE('',*,*,#4707,.F.);
#6178=ORIENTED_EDGE('',*,*,#4710,.F.);
#6179=ORIENTED_EDGE('',*,*,#4713,.F.);
#6180=ORIENTED_EDGE('',*,*,#4716,.F.);
#6181=ORIENTED_EDGE('',*,*,#4717,.F.);
#6182=ORIENTED_EDGE('',*,*,#4718,.F.);
#6183=ORIENTED_EDGE('',*,*,#4719,.T.);
#6184=ORIENTED_EDGE('',*,*,#4717,.T.);
#6185=ORIENTED_EDGE('',*,*,#4719,.F.);
#6186=ORIENTED_EDGE('',*,*,#4720,.F.);
#6187=ORIENTED_EDGE('',*,*,#4721,.T.);
#6188=ORIENTED_EDGE('',*,*,#4718,.T.);
#6189=ORIENTED_EDGE('',*,*,#4721,.F.);
#6190=ORIENTED_EDGE('',*,*,#4722,.F.);
#6191=ORIENTED_EDGE('',*,*,#4723,.T.);
#6192=ORIENTED_EDGE('',*,*,#4720,.T.);
#6193=ORIENTED_EDGE('',*,*,#4723,.F.);
#6194=ORIENTED_EDGE('',*,*,#4722,.T.);
#6195=ORIENTED_EDGE('',*,*,#4724,.F.);
#6196=ORIENTED_EDGE('',*,*,#4725,.F.);
#6197=ORIENTED_EDGE('',*,*,#4726,.T.);
#6198=ORIENTED_EDGE('',*,*,#4724,.T.);
#6199=ORIENTED_EDGE('',*,*,#4726,.F.);
#6200=ORIENTED_EDGE('',*,*,#4716,.T.);
#6201=ORIENTED_EDGE('',*,*,#4727,.T.);
#6202=ORIENTED_EDGE('',*,*,#4725,.T.);
#6203=ORIENTED_EDGE('',*,*,#4727,.F.);
#7148=CYLINDRICAL_SURFACE('',#8613,0.5);
#7149=CYLINDRICAL_SURFACE('',#8621,0.2942);
#7431=ADVANCED_FACE('',(#1320),#991,.F.);
#7432=ADVANCED_FACE('',(#1321),#992,.F.);
#7433=ADVANCED_FACE('',(#1322),#993,.F.);
#7434=ADVANCED_FACE('',(#1323),#994,.F.);
#7435=ADVANCED_FACE('',(#1324),#995,.F.);
#7436=ADVANCED_FACE('',(#1325),#996,.F.);
#7437=ADVANCED_FACE('',(#1326),#997,.F.);
#7438=ADVANCED_FACE('',(#1327),#998,.F.);
#7439=ADVANCED_FACE('',(#1328),#999,.F.);
#7440=ADVANCED_FACE('',(#1329),#1000,.T.);
#7441=ADVANCED_FACE('',(#1330),#429,.T.);
#7442=ADVANCED_FACE('',(#1331),#7148,.T.);
#7443=ADVANCED_FACE('',(#1332),#430,.T.);
#7444=ADVANCED_FACE('',(#1333,#813),#1001,.T.);
#7445=ADVANCED_FACE('',(#1334),#431,.T.);
#7446=ADVANCED_FACE('',(#1335),#7149,.T.);
#7670=CLOSED_SHELL('',(#7431,#7432,#7433,#7434,#7435,#7436,#7437,#7438));
#7671=CLOSED_SHELL('',(#7439,#7440,#7441,#7442,#7443,#7444,#7445,#7446));
#8598=AXIS2_PLACEMENT_3D('',#12726,#10358,#10359);
#8599=AXIS2_PLACEMENT_3D('',#12727,#10360,#10361);
#8600=AXIS2_PLACEMENT_3D('',#12736,#10366,#10367);
#8601=AXIS2_PLACEMENT_3D('',#12742,#10371,#10372);
#8602=AXIS2_PLACEMENT_3D('',#12748,#10376,#10377);
#8603=AXIS2_PLACEMENT_3D('',#12754,#10381,#10382);
#8604=AXIS2_PLACEMENT_3D('',#12760,#10386,#10387);
#8605=AXIS2_PLACEMENT_3D('',#12763,#10390,#10391);
#8606=AXIS2_PLACEMENT_3D('',#12764,#10392,#10393);
#8607=AXIS2_PLACEMENT_3D('',#12765,#10394,#10395);
#8608=AXIS2_PLACEMENT_3D('',#12767,#10396,#10397);
#8609=AXIS2_PLACEMENT_3D('',#12768,#10398,#10399);
#8610=AXIS2_PLACEMENT_3D('',#12770,#10400,#10401);
#8611=AXIS2_PLACEMENT_3D('',#12771,#10402,#10403);
#8612=AXIS2_PLACEMENT_3D('',#12773,#10404,#10405);
#8613=AXIS2_PLACEMENT_3D('',#12775,#10407,#10408);
#8614=AXIS2_PLACEMENT_3D('',#12777,#10409,#10410);
#8615=AXIS2_PLACEMENT_3D('',#12779,#10412,#10413);
#8616=AXIS2_PLACEMENT_3D('',#12781,#10414,#10415);
#8617=AXIS2_PLACEMENT_3D('',#12783,#10417,#10418);
#8618=AXIS2_PLACEMENT_3D('',#12785,#10419,#10420);
#8619=AXIS2_PLACEMENT_3D('',#12786,#10421,#10422);
#8620=AXIS2_PLACEMENT_3D('',#12788,#10423,#10424);
#8621=AXIS2_PLACEMENT_3D('',#12790,#10426,#10427);
#10358=DIRECTION('axis',(0.,0.,1.));
#10359=DIRECTION('refdir',(1.,0.,0.));
#10360=DIRECTION('center_axis',(0.866025403784439,0.,-0.5));
#10361=DIRECTION('ref_axis',(0.5,0.,0.866025403784439));
#10362=DIRECTION('',(-0.5,0.,-0.866025403784439));
#10363=DIRECTION('',(0.,-1.,0.));
#10364=DIRECTION('',(0.5,0.,0.866025403784439));
#10365=DIRECTION('',(0.,-1.,0.));
#10366=DIRECTION('center_axis',(1.92296268638356E-16,0.,-1.));
#10367=DIRECTION('ref_axis',(1.,0.,1.92296268638356E-16));
#10368=DIRECTION('',(-1.,0.,-1.92296268638356E-16));
#10369=DIRECTION('',(0.,-1.,0.));
#10370=DIRECTION('',(1.,0.,1.92296268638356E-16));
#10371=DIRECTION('center_axis',(-0.866025403784439,0.,-0.5));
#10372=DIRECTION('ref_axis',(0.5,0.,-0.866025403784439));
#10373=DIRECTION('',(-0.5,0.,0.866025403784438));
#10374=DIRECTION('',(0.,-1.,0.));
#10375=DIRECTION('',(0.5,0.,-0.866025403784438));
#10376=DIRECTION('center_axis',(-0.866025403784439,0.,0.5));
#10377=DIRECTION('ref_axis',(-0.5,0.,-0.866025403784439));
#10378=DIRECTION('',(0.5,0.,0.866025403784439));
#10379=DIRECTION('',(0.,-1.,0.));
#10380=DIRECTION('',(-0.5,0.,-0.866025403784439));
#10381=DIRECTION('center_axis',(-1.92296268638356E-16,0.,1.));
#10382=DIRECTION('ref_axis',(-1.,0.,-1.92296268638356E-16));
#10383=DIRECTION('',(1.,0.,1.92296268638356E-16));
#10384=DIRECTION('',(0.,-1.,0.));
#10385=DIRECTION('',(-1.,0.,-1.92296268638356E-16));
#10386=DIRECTION('center_axis',(0.866025403784439,0.,0.5));
#10387=DIRECTION('ref_axis',(-0.5,0.,0.866025403784439));
#10388=DIRECTION('',(0.5,0.,-0.866025403784439));
#10389=DIRECTION('',(-0.5,0.,0.866025403784439));
#10390=DIRECTION('center_axis',(0.,1.,0.));
#10391=DIRECTION('ref_axis',(1.,0.,0.));
#10392=DIRECTION('center_axis',(0.,-1.,0.));
#10393=DIRECTION('ref_axis',(0.,0.,-1.));
#10394=DIRECTION('center_axis',(0.,1.,0.));
#10395=DIRECTION('ref_axis',(1.,0.,0.));
#10396=DIRECTION('center_axis',(0.,1.,0.));
#10397=DIRECTION('ref_axis',(1.,0.,0.));
#10398=DIRECTION('center_axis',(0.,1.,0.));
#10399=DIRECTION('ref_axis',(0.,0.,1.));
#10400=DIRECTION('center_axis',(0.,-1.,0.));
#10401=DIRECTION('ref_axis',(1.,0.,0.));
#10402=DIRECTION('center_axis',(0.,-1.,0.));
#10403=DIRECTION('ref_axis',(1.,0.,0.));
#10404=DIRECTION('center_axis',(0.,-1.,0.));
#10405=DIRECTION('ref_axis',(1.,0.,0.));
#10406=DIRECTION('',(0.707106781186548,0.707106781186547,8.65956056235494E-17));
#10407=DIRECTION('center_axis',(0.,-1.,0.));
#10408=DIRECTION('ref_axis',(1.,0.,0.));
#10409=DIRECTION('center_axis',(0.,-1.,0.));
#10410=DIRECTION('ref_axis',(1.,0.,0.));
#10411=DIRECTION('',(0.,1.,0.));
#10412=DIRECTION('center_axis',(0.,1.,0.));
#10413=DIRECTION('ref_axis',(1.,0.,0.));
#10414=DIRECTION('center_axis',(0.,-1.,0.));
#10415=DIRECTION('ref_axis',(1.,0.,0.));
#10416=DIRECTION('',(-0.707106781186547,0.707106781186548,-8.65956056235493E-17));
#10417=DIRECTION('center_axis',(0.,-1.,0.));
#10418=DIRECTION('ref_axis',(0.,0.,-1.));
#10419=DIRECTION('center_axis',(0.,-1.,0.));
#10420=DIRECTION('ref_axis',(1.,0.,0.));
#10421=DIRECTION('center_axis',(0.,1.,0.));
#10422=DIRECTION('ref_axis',(1.,0.,0.));
#10423=DIRECTION('center_axis',(0.,1.,0.));
#10424=DIRECTION('ref_axis',(1.,0.,0.));
#10425=DIRECTION('',(-0.447213595499958,0.894427190999916,-5.47678698264203E-17));
#10426=DIRECTION('center_axis',(0.,-1.,0.));
#10427=DIRECTION('ref_axis',(1.,0.,0.));
#10428=DIRECTION('',(0.,1.,0.));
#12726=CARTESIAN_POINT('',(0.,0.,0.));
#12727=CARTESIAN_POINT('Origin',(0.144337567297406,-0.6,-0.25));
#12728=CARTESIAN_POINT('',(0.288675134594813,-0.6,0.));
#12729=CARTESIAN_POINT('',(0.144337567297406,-0.6,-0.25));
#12730=CARTESIAN_POINT('',(0.288675134594813,-0.6,0.));
#12731=CARTESIAN_POINT('',(0.144337567297406,-0.96,-0.25));
#12732=CARTESIAN_POINT('',(0.144337567297406,-0.6,-0.25));
#12733=CARTESIAN_POINT('',(0.288675134594813,-0.96,0.));
#12734=CARTESIAN_POINT('',(0.288675134594813,-0.96,0.));
#12735=CARTESIAN_POINT('',(0.288675134594813,-0.6,0.));
#12736=CARTESIAN_POINT('Origin',(-0.144337567297406,-0.6,-0.25));
#12737=CARTESIAN_POINT('',(-0.144337567297406,-0.6,-0.25));
#12738=CARTESIAN_POINT('',(0.144337567297406,-0.6,-0.25));
#12739=CARTESIAN_POINT('',(-0.144337567297406,-0.96,-0.25));
#12740=CARTESIAN_POINT('',(-0.144337567297406,-0.6,-0.25));
#12741=CARTESIAN_POINT('',(0.144337567297406,-0.96,-0.25));
#12742=CARTESIAN_POINT('Origin',(-0.288675134594813,-0.6,-8.32667268468867E-17));
#12743=CARTESIAN_POINT('',(-0.288675134594813,-0.6,-3.53525079574969E-17));
#12744=CARTESIAN_POINT('',(-0.144337567297406,-0.6,-0.25));
#12745=CARTESIAN_POINT('',(-0.288675134594813,-0.96,-5.55111512312578E-17));
#12746=CARTESIAN_POINT('',(-0.288675134594813,-0.6,-3.53525079574969E-17));
#12747=CARTESIAN_POINT('',(-0.144337567297406,-0.96,-0.25));
#12748=CARTESIAN_POINT('Origin',(-0.144337567297407,-0.6,0.25));
#12749=CARTESIAN_POINT('',(-0.144337567297407,-0.6,0.25));
#12750=CARTESIAN_POINT('',(-0.288675134594813,-0.6,-3.53525079574969E-17));
#12751=CARTESIAN_POINT('',(-0.144337567297407,-0.96,0.25));
#12752=CARTESIAN_POINT('',(-0.144337567297407,-0.6,0.25));
#12753=CARTESIAN_POINT('',(-0.288675134594813,-0.96,-3.53525079574969E-17));
#12754=CARTESIAN_POINT('Origin',(0.144337567297406,-0.6,0.25));
#12755=CARTESIAN_POINT('',(0.144337567297406,-0.6,0.25));
#12756=CARTESIAN_POINT('',(-0.144337567297407,-0.6,0.25));
#12757=CARTESIAN_POINT('',(0.144337567297406,-0.96,0.25));
#12758=CARTESIAN_POINT('',(0.144337567297406,-0.6,0.25));
#12759=CARTESIAN_POINT('',(-0.144337567297407,-0.96,0.25));
#12760=CARTESIAN_POINT('Origin',(0.288675134594813,-0.6,0.));
#12761=CARTESIAN_POINT('',(0.144337567297406,-0.6,0.25));
#12762=CARTESIAN_POINT('',(0.144337567297406,-0.96,0.25));
#12763=CARTESIAN_POINT('Origin',(0.,-0.6,0.));
#12764=CARTESIAN_POINT('Origin',(0.,-0.96,0.));
#12765=CARTESIAN_POINT('Origin',(0.,-1.8,0.));
#12766=CARTESIAN_POINT('',(-0.2942,-1.8,3.60291088309151E-17));
#12767=CARTESIAN_POINT('Origin',(0.,-1.8,0.));
#12768=CARTESIAN_POINT('Origin',(0.45,0.6,0.));
#12769=CARTESIAN_POINT('',(-0.45,0.6,-5.51091059616309E-17));
#12770=CARTESIAN_POINT('Origin',(0.,0.6,0.));
#12771=CARTESIAN_POINT('Origin',(0.,0.575,0.));
#12772=CARTESIAN_POINT('',(-0.5,0.55,-6.12323399573677E-17));
#12773=CARTESIAN_POINT('Origin',(0.,0.55,0.));
#12774=CARTESIAN_POINT('',(-0.475,0.575,-5.81707229594993E-17));
#12775=CARTESIAN_POINT('Origin',(0.,0.29,0.));
#12776=CARTESIAN_POINT('',(-0.5,0.0299999999999998,-6.12323399573677E-17));
#12777=CARTESIAN_POINT('Origin',(0.,0.0299999999999998,0.));
#12778=CARTESIAN_POINT('',(-0.5,0.29,-6.12323399573677E-17));
#12779=CARTESIAN_POINT('Origin',(0.,0.0150000000000001,0.));
#12780=CARTESIAN_POINT('',(-0.47,7.11236625150491E-17,-5.75583995599256E-17));
#12781=CARTESIAN_POINT('Origin',(0.,0.,0.));
#12782=CARTESIAN_POINT('',(-0.485,0.0150000000000001,-5.93953697586466E-17));
#12783=CARTESIAN_POINT('Origin',(0.32,0.,0.));
#12784=CARTESIAN_POINT('',(-0.32,-6.93889390390723E-18,-3.91886975727153E-17));
#12785=CARTESIAN_POINT('Origin',(0.,0.,0.));
#12786=CARTESIAN_POINT('Origin',(0.,-0.02,0.));
#12787=CARTESIAN_POINT('',(-0.2942,-0.0515999999999999,3.60291088309151E-17));
#12788=CARTESIAN_POINT('Origin',(0.,-0.0515999999999999,0.));
#12789=CARTESIAN_POINT('',(-0.31,-0.02,-3.7964050773568E-17));
#12790=CARTESIAN_POINT('Origin',(0.,-1.24,0.));
#12791=CARTESIAN_POINT('',(-0.2942,-1.24,-3.60291088309151E-17));
#14750=UNCERTAINTY_MEASURE_WITH_UNIT(LENGTH_MEASURE(0.001),#14823,
'DISTANCE_ACCURACY_VALUE',
'Maximum model space distance between geometric entities at asserted c
onnectivities');
#14777=UNCERTAINTY_MEASURE_WITH_UNIT(LENGTH_MEASURE(0.001),#14823,
'DISTANCE_ACCURACY_VALUE',
'Maximum model space distance between geometric entities at asserted c
onnectivities');
#14795=(
GEOMETRIC_REPRESENTATION_CONTEXT(3)
GLOBAL_UNCERTAINTY_ASSIGNED_CONTEXT((#14750))
GLOBAL_UNIT_ASSIGNED_CONTEXT((#14823,#14825,#14826))
REPRESENTATION_CONTEXT('','3D')
);
#14822=(
GEOMETRIC_REPRESENTATION_CONTEXT(3)
GLOBAL_UNCERTAINTY_ASSIGNED_CONTEXT((#14777))
GLOBAL_UNIT_ASSIGNED_CONTEXT((#14823,#14825,#14826))
REPRESENTATION_CONTEXT('','3D')
);
#14823=(
LENGTH_UNIT()
NAMED_UNIT(*)
SI_UNIT(.CENTI.,.METRE.)
);
#14825=(
NAMED_UNIT(*)
PLANE_ANGLE_UNIT()
SI_UNIT($,.RADIAN.)
);
#14826=(
NAMED_UNIT(*)
SI_UNIT($,.STERADIAN.)
SOLID_ANGLE_UNIT()
);
#14844=SHAPE_DEFINITION_REPRESENTATION(#14888,#15015);
#14888=PRODUCT_DEFINITION_SHAPE('',$,#15060);
#15015=SHAPE_REPRESENTATION('',(#8598),#14795);
#15042=PRODUCT_DEFINITION_CONTEXT('part definition',#15176,'design');
#15060=PRODUCT_DEFINITION('M6x18 mounting screw','M6x18 mounting screw',
#15104,#15042);
#15104=PRODUCT_DEFINITION_FORMATION('',$,#15195);
#15176=APPLICATION_CONTEXT(
'Core Data for Automotive Mechanical Design Process');
#15177=PRODUCT_CONTEXT('part definition',#15176,'mechanical');
#15195=PRODUCT('M6x18 mounting screw','M6x18 mounting screw',
'M6x18 mounting screw',(#15177));
#15285=COLOUR_RGB('Black',0.12,0.14,0.17);
#15286=FILL_AREA_STYLE_COLOUR('',#15285);
#15287=FILL_AREA_STYLE('',(#15286));
#15288=SURFACE_STYLE_FILL_AREA(#15287);
#15289=SURFACE_SIDE_STYLE('',(#15288));
#15290=SURFACE_STYLE_USAGE(.BOTH.,#15289);
#15291=PRESENTATION_STYLE_ASSIGNMENT((#15290));
ENDSEC;
END-ISO-10303-21;
